ISO-10303-21;
HEADER;
/* Generated by software containing ST-Developer
 * from STEP Tools, Inc. (www.steptools.com) 
 */

FILE_DESCRIPTION(
/* description */ ('Pallet stop with pneumatic fitting'),
/* implementation_level */ '2;1');

FILE_NAME(
/* name */ 'Flat Washer - M5.step',
/* time_stamp */ '2026-10-27T10:51:41-07:00',
/* author */ (''),
/* organization */ (''),
/* preprocessor_version */ 'ST-DEVELOPER v20.2',
/* originating_system */ 'Autodesk Translation Framework v15.17.0.0',
/* authorisation */ '');

FILE_SCHEMA (('AUTOMOTIVE_DESIGN { 1 0 10303 214 3 1 1 }'));
ENDSEC;

DATA;
#10=MECHANICAL_DESIGN_GEOMETRIC_PRESENTATION_REPRESENTATION('',(#380),#10265);
#29=CONICAL_SURFACE('',#5874,0.275,0.785398163397449);
#316=SHAPE_REPRESENTATION_RELATIONSHIP('SRR','None',#10431,#348);
#348=ADVANCED_BREP_SHAPE_REPRESENTATION('',(#411),#10255);
#380=STYLED_ITEM('',(#10662),#411);
#411=MANIFOLD_SOLID_BREP('Body1',#5069);
#525=FACE_BOUND('',#1382,.T.);
#526=FACE_BOUND('',#1385,.T.);
#675=PLANE('',#5879);
#676=PLANE('',#5883);
#959=FACE_OUTER_BOUND('',#1379,.T.);
#960=FACE_OUTER_BOUND('',#1380,.T.);
#961=FACE_OUTER_BOUND('',#1381,.T.);
#962=FACE_OUTER_BOUND('',#1383,.T.);
#963=FACE_OUTER_BOUND('',#1384,.T.);
#1379=EDGE_LOOP('',(#4244,#4245,#4246,#4247));
#1380=EDGE_LOOP('',(#4248,#4249,#4250,#4251));
#1381=EDGE_LOOP('',(#4252));
#1382=EDGE_LOOP('',(#4253));
#1383=EDGE_LOOP('',(#4254,#4255,#4256,#4257));
#1384=EDGE_LOOP('',(#4258));
#1385=EDGE_LOOP('',(#4259));
#1712=LINE('',#9642,#2047);
#1713=LINE('',#9646,#2048);
#1714=LINE('',#9653,#2049);
#2047=VECTOR('',#7199,0.275);
#2048=VECTOR('',#7204,0.265);
#2049=VECTOR('',#7213,0.5);
#2348=CIRCLE('',#5875,0.285);
#2349=CIRCLE('',#5876,0.265);
#2350=CIRCLE('',#5878,0.265);
#2351=CIRCLE('',#5880,0.5);
#2352=CIRCLE('',#5882,0.5);
#2682=VERTEX_POINT('',#9639);
#2683=VERTEX_POINT('',#9641);
#2684=VERTEX_POINT('',#9645);
#2685=VERTEX_POINT('',#9649);
#2686=VERTEX_POINT('',#9652);
#3221=EDGE_CURVE('',#2682,#2682,#2348,.T.);
#3222=EDGE_CURVE('',#2682,#2683,#1712,.T.);
#3223=EDGE_CURVE('',#2683,#2683,#2349,.T.);
#3224=EDGE_CURVE('',#2683,#2684,#1713,.T.);
#3225=EDGE_CURVE('',#2684,#2684,#2350,.T.);
#3226=EDGE_CURVE('',#2685,#2685,#2351,.T.);
#3227=EDGE_CURVE('',#2685,#2686,#1714,.T.);
#3228=EDGE_CURVE('',#2686,#2686,#2352,.T.);
#4244=ORIENTED_EDGE('',*,*,#3221,.T.);
#4245=ORIENTED_EDGE('',*,*,#3222,.T.);
#4246=ORIENTED_EDGE('',*,*,#3223,.T.);
#4247=ORIENTED_EDGE('',*,*,#3222,.F.);
#4248=ORIENTED_EDGE('',*,*,#3223,.F.);
#4249=ORIENTED_EDGE('',*,*,#3224,.T.);
#4250=ORIENTED_EDGE('',*,*,#3225,.T.);
#4251=ORIENTED_EDGE('',*,*,#3224,.F.);
#4252=ORIENTED_EDGE('',*,*,#3226,.T.);
#4253=ORIENTED_EDGE('',*,*,#3221,.F.);
#4254=ORIENTED_EDGE('',*,*,#3226,.F.);
#4255=ORIENTED_EDGE('',*,*,#3227,.T.);
#4256=ORIENTED_EDGE('',*,*,#3228,.T.);
#4257=ORIENTED_EDGE('',*,*,#3227,.F.);
#4258=ORIENTED_EDGE('',*,*,#3228,.F.);
#4259=ORIENTED_EDGE('',*,*,#3225,.F.);
#4710=CYLINDRICAL_SURFACE('',#5877,0.265);
#4711=CYLINDRICAL_SURFACE('',#5881,0.5);
#4954=ADVANCED_FACE('',(#959),#29,.F.);
#4955=ADVANCED_FACE('',(#960),#4710,.F.);
#4956=ADVANCED_FACE('',(#961,#525),#675,.T.);
#4957=ADVANCED_FACE('',(#962),#4711,.T.);
#4958=ADVANCED_FACE('',(#963,#526),#676,.F.);
#5069=CLOSED_SHELL('',(#4954,#4955,#4956,#4957,#4958));
#5873=AXIS2_PLACEMENT_3D('',#9637,#7193,#7194);
#5874=AXIS2_PLACEMENT_3D('',#9638,#7195,#7196);
#5875=AXIS2_PLACEMENT_3D('',#9640,#7197,#7198);
#5876=AXIS2_PLACEMENT_3D('',#9643,#7200,#7201);
#5877=AXIS2_PLACEMENT_3D('',#9644,#7202,#7203);
#5878=AXIS2_PLACEMENT_3D('',#9647,#7205,#7206);
#5879=AXIS2_PLACEMENT_3D('',#9648,#7207,#7208);
#5880=AXIS2_PLACEMENT_3D('',#9650,#7209,#7210);
#5881=AXIS2_PLACEMENT_3D('',#9651,#7211,#7212);
#5882=AXIS2_PLACEMENT_3D('',#9654,#7214,#7215);
#5883=AXIS2_PLACEMENT_3D('',#9655,#7216,#7217);
#7193=DIRECTION('axis',(0.,0.,1.));
#7194=DIRECTION('refdir',(1.,0.,0.));
#7195=DIRECTION('center_axis',(0.,1.,0.));
#7196=DIRECTION('ref_axis',(1.,0.,0.));
#7197=DIRECTION('center_axis',(0.,1.,0.));
#7198=DIRECTION('ref_axis',(1.,0.,0.));
#7199=DIRECTION('',(0.707106781186548,-0.707106781186547,-8.65956056235494E-17));
#7200=DIRECTION('center_axis',(0.,-1.,0.));
#7201=DIRECTION('ref_axis',(1.,0.,0.));
#7202=DIRECTION('center_axis',(0.,1.,0.));
#7203=DIRECTION('ref_axis',(1.,0.,0.));
#7204=DIRECTION('',(0.,-1.,0.));
#7205=DIRECTION('center_axis',(0.,-1.,0.));
#7206=DIRECTION('ref_axis',(1.,0.,0.));
#7207=DIRECTION('center_axis',(0.,1.,0.));
#7208=DIRECTION('ref_axis',(1.,0.,0.));
#7209=DIRECTION('center_axis',(0.,1.,0.));
#7210=DIRECTION('ref_axis',(1.,0.,0.));
#7211=DIRECTION('center_axis',(0.,1.,0.));
#7212=DIRECTION('ref_axis',(1.,0.,0.));
#7213=DIRECTION('',(0.,-1.,0.));
#7214=DIRECTION('center_axis',(0.,1.,0.));
#7215=DIRECTION('ref_axis',(1.,0.,0.));
#7216=DIRECTION('center_axis',(0.,1.,0.));
#7217=DIRECTION('ref_axis',(1.,0.,0.));
#9637=CARTESIAN_POINT('',(0.,0.,0.));
#9638=CARTESIAN_POINT('Origin',(0.,0.09,0.));
#9639=CARTESIAN_POINT('',(-0.285,0.1,3.49024337756996E-17));
#9640=CARTESIAN_POINT('Origin',(0.,0.1,0.));
#9641=CARTESIAN_POINT('',(-0.265,0.08,-3.24531401774049E-17));
#9642=CARTESIAN_POINT('',(-0.275,0.09,3.36777869765522E-17));
#9643=CARTESIAN_POINT('Origin',(0.,0.08,0.));
#9644=CARTESIAN_POINT('Origin',(0.,0.,0.));
#9645=CARTESIAN_POINT('',(-0.265,0.,3.24531401774049E-17));
#9646=CARTESIAN_POINT('',(-0.265,0.,3.24531401774049E-17));
#9647=CARTESIAN_POINT('Origin',(0.,0.,0.));
#9648=CARTESIAN_POINT('Origin',(0.,0.1,0.));
#9649=CARTESIAN_POINT('',(-0.5,0.1,6.12323399573677E-17));
#9650=CARTESIAN_POINT('Origin',(0.,0.1,0.));
#9651=CARTESIAN_POINT('Origin',(0.,0.,0.));
#9652=CARTESIAN_POINT('',(-0.5,0.,6.12323399573677E-17));
#9653=CARTESIAN_POINT('',(-0.5,0.,6.12323399573677E-17));
#9654=CARTESIAN_POINT('Origin',(0.,0.,0.));
#9655=CARTESIAN_POINT('Origin',(0.,0.,0.));
#10217=UNCERTAINTY_MEASURE_WITH_UNIT(LENGTH_MEASURE(0.001),#10266,
'DISTANCE_ACCURACY_VALUE',
'Maximum model space distance between geometric entities at asserted c
onnectivities');
#10227=UNCERTAINTY_MEASURE_WITH_UNIT(LENGTH_MEASURE(0.001),#10266,
'DISTANCE_ACCURACY_VALUE',
'Maximum model space distance between geometric entities at asserted c
onnectivities');
#10255=(
GEOMETRIC_REPRESENTATION_CONTEXT(3)
GLOBAL_UNCERTAINTY_ASSIGNED_CONTEXT((#10217))
GLOBAL_UNIT_ASSIGNED_CONTEXT((#10266,#10268,#10269))
REPRESENTATION_CONTEXT('','3D')
);
#10265=(
GEOMETRIC_REPRESENTATION_CONTEXT(3)
GLOBAL_UNCERTAINTY_ASSIGNED_CONTEXT((#10227))
GLOBAL_UNIT_ASSIGNED_CONTEXT((#10266,#10268,#10269))
REPRESENTATION_CONTEXT('','3D')
);
#10266=(
LENGTH_UNIT()
NAMED_UNIT(*)
SI_UNIT(.CENTI.,.METRE.)
);
#10268=(
NAMED_UNIT(*)
PLANE_ANGLE_UNIT()
SI_UNIT($,.RADIAN.)
);
#10269=(
NAMED_UNIT(*)
SI_UNIT($,.STERADIAN.)
SOLID_ANGLE_UNIT()
);
#10297=SHAPE_DEFINITION_REPRESENTATION(#10338,#10431);
#10338=PRODUCT_DEFINITION_SHAPE('',$,#10469);
#10431=SHAPE_REPRESENTATION('',(#5873),#10255);
#10441=PRODUCT_DEFINITION_CONTEXT('part definition',#10554,'design');
#10469=PRODUCT_DEFINITION('Flat Washer - M5','Flat Washer - M5',#10506,
#10441);
#10506=PRODUCT_DEFINITION_FORMATION('',$,#10583);
#10554=APPLICATION_CONTEXT(
'Core Data for Automotive Mechanical Design Process');
#10555=PRODUCT_CONTEXT('part definition',#10554,'mechanical');
#10583=PRODUCT('Flat Washer - M5','Flat Washer - M5','Flat Washer - M5',
(#10555));
#10656=COLOUR_RGB('Black',0.12,0.14,0.17);
#10657=FILL_AREA_STYLE_COLOUR('',#10656);
#10658=FILL_AREA_STYLE('',(#10657));
#10659=SURFACE_STYLE_FILL_AREA(#10658);
#10660=SURFACE_SIDE_STYLE('',(#10659));
#10661=SURFACE_STYLE_USAGE(.BOTH.,#10660);
#10662=PRESENTATION_STYLE_ASSIGNMENT((#10661));
ENDSEC;
END-ISO-10303-21;
